ISO-10303-21;
HEADER;
FILE_DESCRIPTION (('STEP AP214'),
    '1' );
FILE_NAME ('hex bolt gradeab_iso_ISO 4014 - M12 x 50 x 30-N.step',
    '2026-10-06T09:36:00',
    ( '' ),
    ( '' ),
    'SwSTEP 2.0',
    'SolidWorks 2025',
    '' );
FILE_SCHEMA (( 'AUTOMOTIVE_DESIGN' ));
ENDSEC;

DATA;
#7=DIRECTION ( 'NONE',  ( 0.000000000000000000, 0.000000000000000000, 1.000000000000000000 ) ) ;
#11=EDGE_CURVE ( 'NONE', #3523, #3290, #9059, .T. ) ;
#25=ORIENTED_EDGE ( 'NONE', *, *, #6395, .T. ) ;
#46=DIRECTION ( 'NONE',  ( -0.7071067811865526798, 0.000000000000000000, 0.7071067811865423547 ) ) ;
#68=EDGE_CURVE ( 'NONE', #11346, #11763, #11644, .T. ) ;
#71=CARTESIAN_POINT ( 'NONE',  ( 6.899999999999999467, -7.794228634059934713, 4.500000000000015987 ) ) ;
#76=AXIS2_PLACEMENT_3D ( 'NONE', #1140, #8678, #11512 ) ;
#96=VECTOR ( 'NONE', #2050, 1000.000000000000000 ) ;
#106=CARTESIAN_POINT ( 'NONE',  ( 0.09252763182291999511, -8.674330214978049014, -2.975619346028157697 ) ) ;
#144=SHAPE_DEFINITION_REPRESENTATION ( #1806, #1102 ) ;
#188=CARTESIAN_POINT ( 'NONE',  ( 0.000000000000000000, 0.000000000000000000, 0.000000000000000000 ) ) ;
#196=LINE ( 'NONE', #11401, #4433 ) ;
#209=CARTESIAN_POINT ( 'NONE',  ( 0.1482032042081581624, 2.204400401829194056, -9.000000000000001776 ) ) ;
#225=EDGE_LOOP ( 'NONE', ( #261, #5060, #2254, #7295, #1076, #408 ) ) ;
#246=DIRECTION ( 'NONE',  ( 0.000000000000000000, 0.000000000000000000, -1.000000000000000000 ) ) ;
#260=EDGE_LOOP ( 'NONE', ( #3241, #8071, #5792, #1069 ) ) ;
#261=ORIENTED_EDGE ( 'NONE', *, *, #5093, .F. ) ;
#264=ORIENTED_EDGE ( 'NONE', *, *, #2535, .T. ) ;
#267=CIRCLE ( 'NONE', #6597, 5.035999999999999588 ) ;
#280=PRESENTATION_STYLE_ASSIGNMENT (( #11725 ) ) ;
#296=AXIS2_PLACEMENT_3D ( 'NONE', #7544, #3832, #1922 ) ;
#343=( NAMED_UNIT ( * ) PLANE_ANGLE_UNIT ( ) SI_UNIT ( $, .RADIAN. ) );
#389=EDGE_CURVE ( 'NONE', #4400, #11584, #1104, .T. ) ;
#390=DIRECTION ( 'NONE',  ( 0.000000000000000000, 0.000000000000000000, -1.000000000000000000 ) ) ;
#392=CARTESIAN_POINT ( 'NONE',  ( 0.07661102881317549684, 6.914460432017338398, 6.023803224821312696 ) ) ;
#407=FACE_OUTER_BOUND ( 'NONE', #12097, .T. ) ;
#408=ORIENTED_EDGE ( 'NONE', *, *, #9663, .F. ) ;
#412=AXIS2_PLACEMENT_3D ( 'NONE', #9186, #721, #4497 ) ;
#426=APPLICATION_CONTEXT ( 'automotive_design' ) ;
#438=CARTESIAN_POINT ( 'NONE',  ( 0.000000000000000000, 1.502314598737159426E-15, -9.000000000000000000 ) ) ;
#445=DIRECTION ( 'NONE',  ( 0.000000000000000000, 0.000000000000000000, -1.000000000000000000 ) ) ;
#470=CARTESIAN_POINT ( 'NONE',  ( 7.500000000000000000, 5.196152422706624918, 8.999999999999998224 ) ) ;
#472=DIRECTION ( 'NONE',  ( -1.000000000000000000, -0.000000000000000000, -0.000000000000000000 ) ) ;
#487=ORIENTED_EDGE ( 'NONE', *, *, #11842, .T. ) ;
#489=CARTESIAN_POINT ( 'NONE',  ( 0.5595136366802130334, -4.349754824395698272, 9.000000000000000000 ) ) ;
#504=EDGE_CURVE ( 'NONE', #9388, #1374, #2263, .T. ) ;
#509=PRODUCT_DEFINITION_FORMATION_WITH_SPECIFIED_SOURCE ( 'ANY', '', #2792, .NOT_KNOWN. ) ;
#607=B_SPLINE_CURVE_WITH_KNOTS ( 'NONE', 3,
 ( #7578, #11349, #8864, #209, #10602, #5906, #1215, #438 ),
 .UNSPECIFIED., .F., .F.,
 ( 4, 2, 2, 4 ),
 ( 0.02518894968643274959, 0.02782118486451494455, 0.02913730245355604029, 0.03045342004259713950 ),
 .UNSPECIFIED. ) ;
#639=EDGE_CURVE ( 'NONE', #5893, #11020, #8714, .T. ) ;
#641=CARTESIAN_POINT ( 'NONE',  ( 0.8038475772933552088, -5.196152422706605378, 8.999999999999998224 ) ) ;
#649=PLANE ( 'NONE',  #9390 ) ;
#655=CARTESIAN_POINT ( 'NONE',  ( 0.1469846612282483256, 8.891930899535424260, 2.598723904613015723 ) ) ;
#669=DIRECTION ( 'NONE',  ( 0.000000000000000000, 0.000000000000000000, -1.000000000000000000 ) ) ;
#678=CARTESIAN_POINT ( 'NONE',  ( 6.899999999999999467, -10.39230484541326405, 0.000000000000000000 ) ) ;
#680=CIRCLE ( 'NONE', #10546, 8.999999999999998224 ) ;
#691=ORIENTED_EDGE ( 'NONE', *, *, #2021, .F. ) ;
#705=FACE_BOUND ( 'NONE', #3097, .T. ) ;
#716=ORIENTED_EDGE ( 'NONE', *, *, #5872, .T. ) ;
#721=DIRECTION ( 'NONE',  ( -1.000000000000000000, -0.000000000000000000, -0.000000000000000000 ) ) ;
#738=CONICAL_SURFACE ( 'NONE', #4100, 9.000000000000000000, 1.047197551196600296 ) ;
#745=CARTESIAN_POINT ( 'NONE',  ( 0.5584673446549162090, 9.967293815311100147, -0.7361406979141390527 ) ) ;
#746=CARTESIAN_POINT ( 'NONE',  ( 0.3570196857253447043, 6.047589086024988347, -7.525268439705680379 ) ) ;
#759=VERTEX_POINT ( 'NONE', #7445 ) ;
#772=DIRECTION ( 'NONE',  ( 1.000000000000000000, 0.000000000000000000, -0.000000000000000000 ) ) ;
#775=AXIS2_PLACEMENT_3D ( 'NONE', #5067, #5187, #3271 ) ;
#793=EDGE_CURVE ( 'NONE', #6696, #8838, #10230, .T. ) ;
#816=CARTESIAN_POINT ( 'NONE',  ( 0.5590800469813590468, 5.620102221249812402, -8.265697409064609147 ) ) ;
#840=PLANE ( 'NONE',  #2310 ) ;
#844=DIRECTION ( 'NONE',  ( -0.7071067811865526798, 8.659560562354869996E-17, -0.7071067811865423547 ) ) ;
#880=CARTESIAN_POINT ( 'NONE',  ( 0.1469846612282468268, 6.696526368584462041, -6.401276095386994491 ) ) ;
#904=EDGE_CURVE ( 'NONE', #8838, #7471, #2559, .T. ) ;
#937=DIRECTION ( 'NONE',  ( -1.000000000000000000, -0.000000000000000000, 0.000000000000000000 ) ) ;
#959=EDGE_CURVE ( 'NONE', #6830, #3523, #9629, .T. ) ;
#993=DIRECTION ( 'NONE',  ( -1.000000000000000000, -0.000000000000000000, -0.000000000000000000 ) ) ;
#1008=LINE ( 'NONE', #3962, #3248 ) ;
#1012=ORIENTED_EDGE ( 'NONE', *, *, #12147, .T. ) ;
#1016=APPLICATION_CONTEXT ( 'automotive_design' ) ;
#1023=CARTESIAN_POINT ( 'NONE',  ( 0.8038475772931109598, -5.196152422707023710, -9.000000000000001776 ) ) ;
#1037=DIRECTION ( 'NONE',  ( -1.000000000000000000, -0.000000000000000000, -0.000000000000000000 ) ) ;
#1038=CARTESIAN_POINT ( 'NONE',  ( 6.899999999999999467, 8.999999999999998224, 0.000000000000000000 ) ) ;
#1043=DIRECTION ( 'NONE',  ( 0.000000000000000000, 0.000000000000000000, 1.000000000000000000 ) ) ;
#1069=ORIENTED_EDGE ( 'NONE', *, *, #2927, .T. ) ;
#1076=ORIENTED_EDGE ( 'NONE', *, *, #1114, .F. ) ;
#1089=CARTESIAN_POINT ( 'NONE',  ( 0.3563104543936067015, -6.049278984716129237, -7.522341449313000972 ) ) ;
#1102=SHAPE_REPRESENTATION ( 'hex bolt gradeab_iso_ISO 4014 - M12 x 50 x 30-N', ( #11957 ), #5648 ) ;
#1104=LINE ( 'NONE', #10488, #4923 ) ;
#1111=( GEOMETRIC_REPRESENTATION_CONTEXT ( 3 ) GLOBAL_UNCERTAINTY_ASSIGNED_CONTEXT ( ( #2261 ) ) GLOBAL_UNIT_ASSIGNED_CONTEXT ( ( #7770, #343, #2439 ) ) REPRESENTATION_CONTEXT ( 'NONE', 'WORKASPACE' ) );
#1114=EDGE_CURVE ( 'NONE', #1499, #12174, #8297, .T. ) ;
#1134=CARTESIAN_POINT ( 'NONE',  ( 8.099999999999999645, 7.347880794884118750E-16, -5.999999999999999112 ) ) ;
#1140=CARTESIAN_POINT ( 'NONE',  ( 8.099999999999999645, 0.000000000000000000, 0.000000000000000000 ) ) ;
#1154=ORIENTED_EDGE ( 'NONE', *, *, #7435, .T. ) ;
#1155=DIRECTION ( 'NONE',  ( 0.000000000000000000, 0.000000000000000000, 1.000000000000000000 ) ) ;
#1169=SURFACE_SIDE_STYLE ('',( #10552 ) ) ;
#1177=LINE ( 'NONE', #5924, #11327 ) ;
#1215=CARTESIAN_POINT ( 'NONE',  ( 4.781971561110112670E-16, 0.4400770685300993690, -9.000000000000003553 ) ) ;
#1246=EDGE_CURVE ( 'NONE', #11584, #8092, #6169, .T. ) ;
#1253=DIRECTION ( 'NONE',  ( 0.000000000000000000, 0.000000000000000000, 1.000000000000000000 ) ) ;
#1282=CIRCLE ( 'NONE', #6206, 6.599999999999998757 ) ;
#1321=DIRECTION ( 'NONE',  ( 0.000000000000000000, 1.224646799147353207E-16, 1.000000000000000000 ) ) ;
#1326=CARTESIAN_POINT ( 'NONE',  ( 6.899999999999999467, -5.196152422706638241, -9.000000000000001776 ) ) ;
#1347=PLANE ( 'NONE',  #12013 ) ;
#1357=ORIENTED_EDGE ( 'NONE', *, *, #9119, .T. ) ;
#1365=EDGE_LOOP ( 'NONE', ( #487, #8976, #6117 ) ) ;
#1374=VERTEX_POINT ( 'NONE', #6856 ) ;
#1383=ORIENTED_EDGE ( 'NONE', *, *, #9854, .F. ) ;
#1426=VECTOR ( 'NONE', #7389, 1000.000000000000000 ) ;
#1456=FACE_OUTER_BOUND ( 'NONE', #5053, .T. ) ;
#1499=VERTEX_POINT ( 'NONE', #11826 ) ;
#1527=ADVANCED_FACE ( 'NONE', ( #1753 ), #6197, .F. ) ;
#1528=CONICAL_SURFACE ( 'NONE', #7858, 9.000000000000000000, 1.047197551196600296 ) ;
#1570=CARTESIAN_POINT ( 'NONE',  ( 0.8038475772933606489, 5.196152422706624918, 8.999999999999998224 ) ) ;
#1582=CARTESIAN_POINT ( 'NONE',  ( 0.5590800469813623774, 9.968355046870078340, 0.7343025909353934066 ) ) ;
#1591=AXIS2_PLACEMENT_3D ( 'NONE', #3125, #11841, #445 ) ;
#1593=DIRECTION ( 'NONE',  ( 0.000000000000000000, -0.5000000000000018874, -0.8660254037844375974 ) ) ;
#1598=ORIENTED_EDGE ( 'NONE', *, *, #5093, .T. ) ;
#1604=CARTESIAN_POINT ( 'NONE',  ( 0.09252763182291810773, 6.914127053141843504, -6.024380653971841859 ) ) ;
#1606=PLANE ( 'NONE',  #8199 ) ;
#1610=ADVANCED_FACE ( 'NONE', ( #9701 ), #8887, .F. ) ;
#1626=ORIENTED_EDGE ( 'NONE', *, *, #1246, .F. ) ;
#1646=FACE_OUTER_BOUND ( 'NONE', #8624, .T. ) ;
#1668=AXIS2_PLACEMENT_3D ( 'NONE', #4762, #7721, #9401 ) ;
#1732=DIRECTION ( 'NONE',  ( 0.000000000000000000, 0.000000000000000000, -1.000000000000000000 ) ) ;
#1734=CIRCLE ( 'NONE', #3292, 5.035999999999999588 ) ;
#1753=FACE_OUTER_BOUND ( 'NONE', #5904, .T. ) ;
#1763=CARTESIAN_POINT ( 'NONE',  ( 0.09318607064769238169, 1.767053008364804834, 9.000000000000000000 ) ) ;
#1776=CARTESIAN_POINT ( 'NONE',  ( 6.899999999999999467, 8.999999999999998224, 0.000000000000000000 ) ) ;
#1785=EDGE_LOOP ( 'NONE', ( #8641, #2412, #6566 ) ) ;
#1789=DIRECTION ( 'NONE',  ( -1.000000000000000000, -0.000000000000000000, -0.000000000000000000 ) ) ;
#1801=CARTESIAN_POINT ( 'NONE',  ( -6.500766111939939161E-15, 7.573738413550457516, -4.881900264494495545 ) ) ;
#1806=PRODUCT_DEFINITION_SHAPE ( 'NONE', 'NONE',  #3674 ) ;
#1813=VERTEX_POINT ( 'NONE', #5472 ) ;
#1871=ORIENTED_EDGE ( 'NONE', *, *, #2513, .T. ) ;
#1877=CARTESIAN_POINT ( 'NONE',  ( 8.099999999999999645, 0.000000000000000000, 0.000000000000000000 ) ) ;
#1879=ORIENTED_EDGE ( 'NONE', *, *, #6839, .T. ) ;
#1894=EDGE_LOOP ( 'NONE', ( #5076, #264, #7551, #11726, #10183, #6058 ) ) ;
#1907=ORIENTED_EDGE ( 'NONE', *, *, #6600, .F. ) ;
#1922=DIRECTION ( 'NONE',  ( 0.000000000000000000, 0.000000000000000000, -1.000000000000000000 ) ) ;
#1939=DIRECTION ( 'NONE',  ( 0.000000000000000000, -1.000000000000000000, -1.669238443041288415E-16 ) ) ;
#1948=CARTESIAN_POINT ( 'NONE',  ( -3.506716401632803404E-15, -7.351593252548093815, -5.266666970006169457 ) ) ;
#1949=CARTESIAN_POINT ( 'NONE',  ( 7.500000000000000000, 1.102182119232617517E-15, -8.999999999999998224 ) ) ;
#1962=CARTESIAN_POINT ( 'NONE',  ( 6.899999999999999467, 8.999999999999998224, 0.000000000000000000 ) ) ;
#1977=FACE_OUTER_BOUND ( 'NONE', #4833, .T. ) ;
#2000=DIRECTION ( 'NONE',  ( 0.000000000000000000, 0.000000000000000000, -1.000000000000000000 ) ) ;
#2020=PLANE ( 'NONE',  #8399 ) ;
#2021=EDGE_CURVE ( 'NONE', #4400, #6830, #5349, .T. ) ;
#2050=DIRECTION ( 'NONE',  ( -0.000000000000000000, 0.5000000000000009992, 0.8660254037844380415 ) ) ;
#2064=VERTEX_POINT ( 'NONE', #10365 ) ;
#2125=ORIENTED_EDGE ( 'NONE', *, *, #6530, .F. ) ;
#2148=ORIENTED_EDGE ( 'NONE', *, *, #8496, .F. ) ;
#2150=ORIENTED_EDGE ( 'NONE', *, *, #5872, .F. ) ;
#2154=ORIENTED_EDGE ( 'NONE', *, *, #793, .F. ) ;
#2182=CARTESIAN_POINT ( 'NONE',  ( 6.899999999999999467, 8.999999999999998224, 0.000000000000000000 ) ) ;
#2183=CARTESIAN_POINT ( 'NONE',  ( 0.000000000000000000, -7.794228634059935601, 4.500000000000016875 ) ) ;
#2209=DIRECTION ( 'NONE',  ( 0.000000000000000000, 0.5000000000000009992, -0.8660254037844380415 ) ) ;
#2214=VERTEX_POINT ( 'NONE', #3354 ) ;
#2230=AXIS2_PLACEMENT_3D ( 'NONE', #12204, #3728, #7 ) ;
#2254=ORIENTED_EDGE ( 'NONE', *, *, #4322, .F. ) ;
#2259=FACE_OUTER_BOUND ( 'NONE', #1365, .T. ) ;
#2261=UNCERTAINTY_MEASURE_WITH_UNIT (LENGTH_MEASURE( 1.000000000000000082E-05 ), #7770, 'distance_accuracy_value', 'NONE');
#2263=LINE ( 'NONE', #7896, #4761 ) ;
#2279=CARTESIAN_POINT ( 'NONE',  ( 0.000000000000000000, 1.502314598737159426E-15, -9.000000000000000000 ) ) ;
#2293=CARTESIAN_POINT ( 'NONE',  ( 0.8038475772931109598, -5.196152422707023710, -9.000000000000001776 ) ) ;
#2309=VERTEX_POINT ( 'NONE', #7442 ) ;
#2310=AXIS2_PLACEMENT_3D ( 'NONE', #10161, #4546, #6327 ) ;
#2336=CONICAL_SURFACE ( 'NONE', #7663, 5.035999999999999588, 0.7853981633974410625 ) ;
#2373=EDGE_LOOP ( 'NONE', ( #10806, #8204, #9866 ) ) ;
#2392=CARTESIAN_POINT ( 'NONE',  ( 5.717472393966525317E-16, -0.8794428697676625051, -9.000000000000000000 ) ) ;
#2396=CARTESIAN_POINT ( 'NONE',  ( 0.000000000000000000, 0.000000000000000000, 0.000000000000000000 ) ) ;
#2398=CARTESIAN_POINT ( 'NONE',  ( 0.000000000000000000, 0.000000000000000000, 0.000000000000000000 ) ) ;
#2412=ORIENTED_EDGE ( 'NONE', *, *, #6530, .T. ) ;
#2425=DIRECTION ( 'NONE',  ( -1.000000000000000000, -0.000000000000000000, -0.000000000000000000 ) ) ;
#2426=CARTESIAN_POINT ( 'NONE',  ( 0.000000000000000000, 0.000000000000000000, 0.000000000000000000 ) ) ;
#2439=( NAMED_UNIT ( * ) SI_UNIT ( $, .STERADIAN. ) SOLID_ANGLE_UNIT ( ) );
#2443=CARTESIAN_POINT ( 'NONE',  ( 7.500000000000000000, -10.39230484541326405, 0.000000000000000000 ) ) ;
#2460=LINE ( 'NONE', #8095, #4186 ) ;
#2461=CARTESIAN_POINT ( 'NONE',  ( 6.899999999999999467, 1.502314598737159228E-15, -8.999999999999998224 ) ) ;
#2472=CARTESIAN_POINT ( 'NONE',  ( 0.000000000000000000, 7.794228634059941818, -4.500000000000007994 ) ) ;
#2487=EDGE_LOOP ( 'NONE', ( #10512, #7994, #9213, #5958, #2585, #6915 ) ) ;
#2494=CARTESIAN_POINT ( 'NONE',  ( 8.099999999999999645, 0.000000000000000000, 0.000000000000000000 ) ) ;
#2513=EDGE_CURVE ( 'NONE', #9788, #7020, #11491, .T. ) ;
#2519=PLANE ( 'NONE',  #5210 ) ;
#2531=CARTESIAN_POINT ( 'NONE',  ( 0.000000000000000000, 7.794228634059941818, -4.500000000000007994 ) ) ;
#2535=EDGE_CURVE ( 'NONE', #2309, #4859, #1177, .T. ) ;
#2549=FACE_OUTER_BOUND ( 'NONE', #6948, .T. ) ;
#2559=LINE ( 'NONE', #3476, #1426 ) ;
#2585=ORIENTED_EDGE ( 'NONE', *, *, #3685, .T. ) ;
#2596=AXIS2_PLACEMENT_3D ( 'NONE', #10863, #4270, #6178 ) ;
#2613=FACE_OUTER_BOUND ( 'NONE', #2487, .T. ) ;
#2626=AXIS2_PLACEMENT_3D ( 'NONE', #8056, #11078, #4287 ) ;
#2632=DIRECTION ( 'NONE',  ( -0.000000000000000000, 0.5000000000000009992, 0.8660254037844380415 ) ) ;
#2635=ORIENTED_EDGE ( 'NONE', *, *, #10768, .T. ) ;
#2656=CARTESIAN_POINT ( 'NONE',  ( 0.000000000000000000, 0.000000000000000000, 0.000000000000000000 ) ) ;
#2681=CARTESIAN_POINT ( 'NONE',  ( 0.3570196857253388201, -6.047589086024968807, 7.525268439705679491 ) ) ;
#2687=ORIENTED_EDGE ( 'NONE', *, *, #9320, .T. ) ;
#2689=( NAMED_UNIT ( * ) SI_UNIT ( $, .STERADIAN. ) SOLID_ANGLE_UNIT ( ) );
#2693=EDGE_CURVE ( 'NONE', #2214, #759, #4500, .T. ) ;
#2704=ORIENTED_EDGE ( 'NONE', *, *, #2693, .F. ) ;
#2725=FACE_OUTER_BOUND ( 'NONE', #1894, .T. ) ;
#2740=ORIENTED_EDGE ( 'NONE', *, *, #68, .T. ) ;
#2748=CARTESIAN_POINT ( 'NONE',  ( 0.000000000000000000, 0.000000000000000000, 9.000000000000000000 ) ) ;
#2764=PLANE ( 'NONE',  #6482 ) ;
#2782=ADVANCED_FACE ( 'NONE', ( #7583 ), #10426, .T. ) ;
#2786=DIRECTION ( 'NONE',  ( 0.000000000000000000, 0.000000000000000000, -1.000000000000000000 ) ) ;
#2792=PRODUCT ( 'hex bolt gradeab_iso_ISO 4014 - M12 x 50 x 30-N', 'hex bolt gradeab_iso_ISO 4014 - M12 x 50 x 30-N', '', ( #5962 ) ) ;
#2826=CIRCLE ( 'NONE', #9729, 8.999999999999998224 ) ;
#2849=CARTESIAN_POINT ( 'NONE',  ( 57.50000000000000000, 6.757601037695094579E-16, -5.035999999999999588 ) ) ;
#2851=AXIS2_PLACEMENT_3D ( 'NONE', #11415, #6716, #1043 ) ;
#2871=FACE_OUTER_BOUND ( 'NONE', #10755, .T. ) ;
#2882=ORIENTED_EDGE ( 'NONE', *, *, #959, .F. ) ;
#2914=ORIENTED_EDGE ( 'NONE', *, *, #11535, .F. ) ;
#2920=DIRECTION ( 'NONE',  ( 1.000000000000000000, 0.000000000000000000, 0.000000000000000000 ) ) ;
#2927=EDGE_CURVE ( 'NONE', #10331, #7471, #6002, .T. ) ;
#2958=CARTESIAN_POINT ( 'NONE',  ( 0.5590800469813614892, -9.968355046870076563, -0.7343025909353910752 ) ) ;
#3017=ORIENTED_EDGE ( 'NONE', *, *, #3788, .T. ) ;
#3042=CARTESIAN_POINT ( 'NONE',  ( 6.899999999999999467, -7.794228634059948924, -4.499999999999995559 ) ) ;
#3046=ORIENTED_EDGE ( 'NONE', *, *, #10330, .T. ) ;
#3061=ORIENTED_EDGE ( 'NONE', *, *, #10937, .F. ) ;
#3097=EDGE_LOOP ( 'NONE', ( #1879, #2740 ) ) ;
#3125=CARTESIAN_POINT ( 'NONE',  ( 7.500000000000000000, 0.000000000000000000, 0.000000000000000000 ) ) ;
#3147=FACE_OUTER_BOUND ( 'NONE', #9025, .T. ) ;
#3203=EDGE_CURVE ( 'NONE', #2309, #6181, #11308, .T. ) ;
#3212=EDGE_CURVE ( 'NONE', #759, #11584, #5704, .T. ) ;
#3241=ORIENTED_EDGE ( 'NONE', *, *, #904, .F. ) ;
#3248=VECTOR ( 'NONE', #11446, 1000.000000000000000 ) ;
#3254=CARTESIAN_POINT ( 'NONE',  ( 0.000000000000000000, -7.794228634059949812, -4.499999999999995559 ) ) ;
#3259=DIRECTION ( 'NONE',  ( -0.000000000000000000, 0.8660254037844389297, 0.4999999999999995004 ) ) ;
#3271=DIRECTION ( 'NONE',  ( 0.000000000000000000, 0.000000000000000000, -1.000000000000000000 ) ) ;
#3272=CARTESIAN_POINT ( 'NONE',  ( 57.50000000000000000, 0.000000000000000000, 0.000000000000000000 ) ) ;
#3280=ORIENTED_EDGE ( 'NONE', *, *, #9725, .T. ) ;
#3282=EDGE_CURVE ( 'NONE', #7020, #10331, #8231, .T. ) ;
#3284=CARTESIAN_POINT ( 'NONE',  ( 8.099999999999999645, 8.082668874372530033E-16, 6.599999999999998757 ) ) ;
#3290=VERTEX_POINT ( 'NONE', #8657 ) ;
#3292=AXIS2_PLACEMENT_3D ( 'NONE', #6416, #3435, #7222 ) ;
#3306=DIRECTION ( 'NONE',  ( 1.000000000000000000, 0.000000000000000000, 0.000000000000000000 ) ) ;
#3325=ORIENTED_EDGE ( 'NONE', *, *, #11937, .T. ) ;
#3345=LINE ( 'NONE', #1326, #11505 ) ;
#3354=CARTESIAN_POINT ( 'NONE',  ( 6.899999999999999467, 5.196152422706624030, -9.000000000000000000 ) ) ;
#3365=CYLINDRICAL_SURFACE ( 'NONE', #412, 8.999999999999998224 ) ;
#3371=CARTESIAN_POINT ( 'NONE',  ( 0.000000000000000000, 0.000000000000000000, 8.999999999999998224 ) ) ;
#3395=B_SPLINE_CURVE_WITH_KNOTS ( 'NONE', 3,
 ( #1570, #11890, #6144, #392, #7132, #11720 ),
 .UNSPECIFIED., .F., .F.,
 ( 4, 2, 4 ),
 ( 2.380730968235596737E-07, 0.002629065763328352224, 0.005257893453559881088 ),
 .UNSPECIFIED. ) ;
#3421=CARTESIAN_POINT ( 'NONE',  ( 0.3570196857253478684, 9.540868182094902394, 1.474731560294324728 ) ) ;
#3426=VECTOR ( 'NONE', #7420, 999.9999999999998863 ) ;
#3435=DIRECTION ( 'NONE',  ( -1.000000000000000000, -0.000000000000000000, -0.000000000000000000 ) ) ;
#3476=CARTESIAN_POINT ( 'NONE',  ( 0.000000000000000000, 7.347880794884118750E-16, -5.999999999999999112 ) ) ;
#3510=CARTESIAN_POINT ( 'NONE',  ( 0.000000000000000000, -7.794228634059935601, 4.500000000000016875 ) ) ;
#3523=VERTEX_POINT ( 'NONE', #3254 ) ;
#3528=EDGE_LOOP ( 'NONE', ( #11057, #11374, #3551 ) ) ;
#3531=CARTESIAN_POINT ( 'NONE',  ( -1.017710086126041463E-15, 0.4400770685579608599, 9.000000000000000000 ) ) ;
#3539=DIRECTION ( 'NONE',  ( 0.000000000000000000, -0.5000000000000009992, -0.8660254037844380415 ) ) ;
#3551=ORIENTED_EDGE ( 'NONE', *, *, #3602, .T. ) ;
#3568=CARTESIAN_POINT ( 'NONE',  ( -6.251103150736736502E-15, 8.236864015571823572, -3.733333029993796792 ) ) ;
#3573=AXIS2_PLACEMENT_3D ( 'NONE', #2398, #9006, #669 ) ;
#3595=CARTESIAN_POINT ( 'NONE',  ( 0.5612050131687977839, 4.355613924421556149, 8.999999999999998224 ) ) ;
#3602=EDGE_CURVE ( 'NONE', #3290, #6830, #7963, .T. ) ;
#3603=EDGE_LOOP ( 'NONE', ( #4056, #3046, #10613 ) ) ;
#3616=ORIENTED_EDGE ( 'NONE', *, *, #11937, .F. ) ;
#3625=CARTESIAN_POINT ( 'NONE',  ( 57.50000000000000000, 0.000000000000000000, 0.000000000000000000 ) ) ;
#3634=DIRECTION ( 'NONE',  ( 0.000000000000000000, 0.000000000000000000, 1.000000000000000000 ) ) ;
#3645=ADVANCED_FACE ( 'NONE', ( #9772 ), #4534, .T. ) ;
#3668=CARTESIAN_POINT ( 'NONE',  ( 0.8038475772933606489, 5.196152422706624918, 8.999999999999998224 ) ) ;
#3674=PRODUCT_DEFINITION ( 'UNKNOWN', '', #509, #6655 ) ;
#3685=EDGE_CURVE ( 'NONE', #5830, #9411, #11636, .T. ) ;
#3712=CIRCLE ( 'NONE', #12000, 9.000000000000000000 ) ;
#3728=DIRECTION ( 'NONE',  ( -1.000000000000000000, -0.000000000000000000, -0.000000000000000000 ) ) ;
#3733=CARTESIAN_POINT ( 'NONE',  ( 0.3593302862868652525, 3.504574740656557275, 9.000000000000001776 ) ) ;
#3736=CARTESIAN_POINT ( 'NONE',  ( 0.07661102881317168045, -6.914460432017388136, -6.023803224821241642 ) ) ;
#3760=LINE ( 'NONE', #8477, #10027 ) ;
#3783=CARTESIAN_POINT ( 'NONE',  ( 7.500000000000000000, 0.000000000000000000, 0.000000000000000000 ) ) ;
#3788=EDGE_CURVE ( 'NONE', #6435, #8054, #7808, .T. ) ;
#3832=DIRECTION ( 'NONE',  ( 1.000000000000000000, 0.000000000000000000, -0.000000000000000000 ) ) ;
#3839=EDGE_CURVE ( 'NONE', #1374, #9727, #4573, .T. ) ;
#3849=PLANE ( 'NONE',  #11735 ) ;
#3864=ORIENTED_EDGE ( 'NONE', *, *, #904, .T. ) ;
#3875=ADVANCED_FACE ( 'NONE', ( #9400 ), #8681, .T. ) ;
#3882=CARTESIAN_POINT ( 'NONE',  ( 0.1469846612282494080, -8.891930899535433142, -2.598723904613006397 ) ) ;
#3962=CARTESIAN_POINT ( 'NONE',  ( 6.899999999999999467, 5.196152422706624030, -9.000000000000000000 ) ) ;
#3970=DIRECTION ( 'NONE',  ( 1.000000000000000000, 0.000000000000000000, 0.000000000000000000 ) ) ;
#4009=B_SPLINE_CURVE_WITH_KNOTS ( 'NONE', 3,
 ( #8241, #8582, #4753, #106, #3882, #7652, #2958, #8308 ),
 .UNSPECIFIED., .F., .F.,
 ( 4, 2, 2, 4 ),
 ( 0.005257893453559894098, 0.006567392922673226906, 0.007876892391786559713, 0.01049589133001322706 ),
 .UNSPECIFIED. ) ;
#4056=ORIENTED_EDGE ( 'NONE', *, *, #6479, .T. ) ;
#4066=ORIENTED_EDGE ( 'NONE', *, *, #11821, .F. ) ;
#4100=AXIS2_PLACEMENT_3D ( 'NONE', #11786, #3306, #9182 ) ;
#4131=AXIS2_PLACEMENT_3D ( 'NONE', #12123, #993, #3634 ) ;
#4160=ORIENTED_EDGE ( 'NONE', *, *, #6087, .F. ) ;
#4186=VECTOR ( 'NONE', #7163, 1000.000000000000000 ) ;
#4195=PLANE ( 'NONE',  #11765 ) ;
#4230=CARTESIAN_POINT ( 'NONE',  ( 8.099999999999999645, 0.000000000000000000, 5.999999999999999112 ) ) ;
#4232=CYLINDRICAL_SURFACE ( 'NONE', #11293, 5.999999999999999112 ) ;
#4247=DIRECTION ( 'NONE',  ( -1.000000000000000000, -0.000000000000000000, -0.000000000000000000 ) ) ;
#4265=DIRECTION ( 'NONE',  ( -1.000000000000000000, 0.000000000000000000, -0.000000000000000000 ) ) ;
#4270=DIRECTION ( 'NONE',  ( 1.000000000000000000, 0.000000000000000000, -0.000000000000000000 ) ) ;
#4271=DIRECTION ( 'NONE',  ( 0.000000000000000000, 0.000000000000000000, 1.000000000000000000 ) ) ;
#4278=CARTESIAN_POINT ( 'NONE',  ( 0.07568653364411878637, -1.751902528157375682, 8.999999999999998224 ) ) ;
#4287=DIRECTION ( 'NONE',  ( -0.000000000000000000, 0.000000000000000000, 1.000000000000000000 ) ) ;
#4290=EDGE_CURVE ( 'NONE', #11388, #6435, #9925, .T. ) ;
#4292=CARTESIAN_POINT ( 'NONE',  ( 0.000000000000000000, 0.000000000000000000, 9.000000000000000000 ) ) ;
#4297=AXIS2_PLACEMENT_3D ( 'NONE', #2396, #6174, #9938 ) ;
#4298=AXIS2_PLACEMENT_3D ( 'NONE', #10693, #2920, #5098 ) ;
#4303=EDGE_LOOP ( 'NONE', ( #3017, #1012, #11828 ) ) ;
#4322=EDGE_CURVE ( 'NONE', #9411, #1374, #5741, .T. ) ;
#4336=DIRECTION ( 'NONE',  ( 0.000000000000000000, 0.8660254037844375974, -0.5000000000000019984 ) ) ;
#4368=CARTESIAN_POINT ( 'NONE',  ( 0.8038475772933666441, 10.39230484541326938, -2.501782431774985704E-16 ) ) ;
#4400=VERTEX_POINT ( 'NONE', #6281 ) ;
#4410=ORIENTED_EDGE ( 'NONE', *, *, #389, .T. ) ;
#4413=ADVANCED_FACE ( 'NONE', ( #5343 ), #2764, .T. ) ;
#4416=VECTOR ( 'NONE', #46, 1000.000000000000000 ) ;
#4417=FACE_OUTER_BOUND ( 'NONE', #6757, .T. ) ;
#4419=FACE_OUTER_BOUND ( 'NONE', #11619, .T. ) ;
#4433=VECTOR ( 'NONE', #8622, 1000.000000000000000 ) ;
#4481=CARTESIAN_POINT ( 'NONE',  ( 0.01885174614965850343, 0.8831628876357843216, 8.999999999999998224 ) ) ;
#4487=CARTESIAN_POINT ( 'NONE',  ( 57.50000000000000000, 6.167321280506070407E-16, -5.035999999999999588 ) ) ;
#4497=DIRECTION ( 'NONE',  ( 0.000000000000000000, 0.000000000000000000, 1.000000000000000000 ) ) ;
#4500=LINE ( 'NONE', #9253, #5201 ) ;
#4502=ADVANCED_FACE ( 'NONE', ( #10420 ), #2336, .T. ) ;
#4511=CIRCLE ( 'NONE', #10235, 8.999999999999998224 ) ;
#4524=CARTESIAN_POINT ( 'NONE',  ( 0.3563104543936356228, 9.539178283403849434, -1.477658550686871353 ) ) ;
#4534=CONICAL_SURFACE ( 'NONE', #775, 9.000000000000000000, 1.047197551196600296 ) ;
#4546=DIRECTION ( 'NONE',  ( 1.000000000000000000, 0.000000000000000000, -0.000000000000000000 ) ) ;
#4559=CARTESIAN_POINT ( 'NONE',  ( 0.09252763182291869060, 8.674330214978045461, 2.975619346028167911 ) ) ;
#4573=B_SPLINE_CURVE_WITH_KNOTS ( 'NONE', 3,
 ( #5430, #745, #4524, #8301, #3568, #2472 ),
 .UNSPECIFIED., .F., .F.,
 ( 4, 2, 4 ),
 ( 2.380730968232385423E-07, 0.002629065763328362199, 0.005257893453559901037 ),
 .UNSPECIFIED. ) ;
#4583=DIRECTION ( 'NONE',  ( -1.000000000000000000, -0.000000000000000000, -0.000000000000000000 ) ) ;
#4612=CARTESIAN_POINT ( 'NONE',  ( 0.09252763182291165456, -6.914127053141829293, 6.024380653971844524 ) ) ;
#4661=CIRCLE ( 'NONE', #8418, 8.999999999999998224 ) ;
#4664=CARTESIAN_POINT ( 'NONE',  ( 6.899999999999999467, 5.196152422706624030, -9.000000000000000000 ) ) ;
#4673=PLANE ( 'NONE',  #5457 ) ;
#4689=DIRECTION ( 'NONE',  ( 0.000000000000000000, 0.000000000000000000, 1.000000000000000000 ) ) ;
#4718=ADVANCED_BREP_SHAPE_REPRESENTATION ( '', ( #11906, #11957 ), #5648 ) ;
#4753=CARTESIAN_POINT ( 'NONE',  ( 0.01899995639453613133, -8.236198097127180873, -3.734486434573621061 ) ) ;
#4761=VECTOR ( 'NONE', #10726, 1000.000000000000000 ) ;
#4762=CARTESIAN_POINT ( 'NONE',  ( 56.53599999999998715, 0.000000000000000000, 0.000000000000000000 ) ) ;
#4781=DIRECTION ( 'NONE',  ( 0.000000000000000000, -1.669238443041288415E-16, 1.000000000000000000 ) ) ;
#4804=ADVANCED_FACE ( 'NONE', ( #1646 ), #3365, .T. ) ;
#4805=ORIENTED_EDGE ( 'NONE', *, *, #1246, .T. ) ;
#4833=EDGE_LOOP ( 'NONE', ( #2154, #2687, #1871, #8872 ) ) ;
#4839=AXIS2_PLACEMENT_3D ( 'NONE', #6353, #10422, #1732 ) ;
#4859=VERTEX_POINT ( 'NONE', #12033 ) ;
#4888=ORIENTED_EDGE ( 'NONE', *, *, #1114, .T. ) ;
#4895=VECTOR ( 'NONE', #5220, 1000.000000000000000 ) ;
#4915=AXIS2_PLACEMENT_3D ( 'NONE', #2656, #7485, #2786 ) ;
#4923=VECTOR ( 'NONE', #5845, 1000.000000000000000 ) ;
#4937=CARTESIAN_POINT ( 'NONE',  ( 0.8038475772931109598, -5.196152422707023710, -9.000000000000001776 ) ) ;
#4945=ORIENTED_EDGE ( 'NONE', *, *, #10768, .F. ) ;
#4954=DIRECTION ( 'NONE',  ( 1.000000000000000000, 0.000000000000000000, 0.000000000000000000 ) ) ;
#4958=ORIENTED_EDGE ( 'NONE', *, *, #7435, .F. ) ;
#4996=LINE ( 'NONE', #3371, #5694 ) ;
#5002=EDGE_CURVE ( 'NONE', #5830, #8054, #7935, .T. ) ;
#5043=CIRCLE ( 'NONE', #5438, 9.000000000000000000 ) ;
#5053=EDGE_LOOP ( 'NONE', ( #9764, #3280, #11707 ) ) ;
#5060=ORIENTED_EDGE ( 'NONE', *, *, #504, .T. ) ;
#5063=EDGE_CURVE ( 'NONE', #9727, #9411, #8902, .T. ) ;
#5066=DIRECTION ( 'NONE',  ( 1.000000000000000000, 0.000000000000000000, -0.000000000000000000 ) ) ;
#5067=CARTESIAN_POINT ( 'NONE',  ( 0.000000000000000000, 0.000000000000000000, 0.000000000000000000 ) ) ;
#5070=CARTESIAN_POINT ( 'NONE',  ( 56.53599999999998715, 7.347880794884118750E-16, -5.999999999999999112 ) ) ;
#5076=ORIENTED_EDGE ( 'NONE', *, *, #3203, .F. ) ;
#5086=CARTESIAN_POINT ( 'NONE',  ( 7.500000000000000000, 0.000000000000000000, 8.999999999999998224 ) ) ;
#5092=CONICAL_SURFACE ( 'NONE', #10826, 5.035999999999999588, 0.7853981633974410625 ) ;
#5093=EDGE_CURVE ( 'NONE', #9388, #2064, #2460, .T. ) ;
#5098=DIRECTION ( 'NONE',  ( 0.000000000000000000, 0.000000000000000000, -1.000000000000000000 ) ) ;
#5110=DIRECTION ( 'NONE',  ( 0.000000000000000000, -0.8660254037844380415, -0.5000000000000009992 ) ) ;
#5115=DIRECTION ( 'NONE',  ( 0.000000000000000000, 0.000000000000000000, -1.000000000000000000 ) ) ;
#5122=EDGE_CURVE ( 'NONE', #6181, #11388, #10003, .T. ) ;
#5132=DIRECTION ( 'NONE',  ( 0.000000000000000000, 0.000000000000000000, 1.000000000000000000 ) ) ;
#5176=EDGE_LOOP ( 'NONE', ( #25, #12049, #8796, #6763 ) ) ;
#5187=DIRECTION ( 'NONE',  ( 1.000000000000000000, 0.000000000000000000, 0.000000000000000000 ) ) ;
#5201=VECTOR ( 'NONE', #2632, 1000.000000000000000 ) ;
#5210=AXIS2_PLACEMENT_3D ( 'NONE', #1962, #10125, #6294 ) ;
#5220=DIRECTION ( 'NONE',  ( -1.000000000000000000, -0.000000000000000000, -0.000000000000000000 ) ) ;
#5250=ADVANCED_FACE ( 'NONE', ( #8065 ), #4232, .T. ) ;
#5254=ORIENTED_EDGE ( 'NONE', *, *, #5002, .T. ) ;
#5262=DIRECTION ( 'NONE',  ( 0.000000000000000000, 0.4999999999999995004, -0.8660254037844389297 ) ) ;
#5285=CARTESIAN_POINT ( 'NONE',  ( 0.000000000000000000, 0.000000000000000000, 0.000000000000000000 ) ) ;
#5308=CARTESIAN_POINT ( 'NONE',  ( 0.07661102881317116697, -8.673996836102535468, 2.976196775178697518 ) ) ;
#5317=ORIENTED_EDGE ( 'NONE', *, *, #7462, .F. ) ;
#5330=CARTESIAN_POINT ( 'NONE',  ( 6.899999999999999467, -10.39230484541326405, 0.000000000000000000 ) ) ;
#5343=FACE_OUTER_BOUND ( 'NONE', #1785, .T. ) ;
#5349=LINE ( 'NONE', #9125, #7565 ) ;
#5398=( NAMED_UNIT ( * ) PLANE_ANGLE_UNIT ( ) SI_UNIT ( $, .RADIAN. ) );
#5418=CARTESIAN_POINT ( 'NONE',  ( 6.899999999999999467, -10.39230484541326405, 0.000000000000000000 ) ) ;
#5430=CARTESIAN_POINT ( 'NONE',  ( 0.8038475772933666441, 10.39230484541326938, -2.501782431774985704E-16 ) ) ;
#5438=AXIS2_PLACEMENT_3D ( 'NONE', #6932, #5066, #246 ) ;
#5457=AXIS2_PLACEMENT_3D ( 'NONE', #9299, #772, #6579 ) ;
#5472=CARTESIAN_POINT ( 'NONE',  ( 0.8038475772933614261, 5.196152422706624030, -9.000000000000000000 ) ) ;
#5499=CARTESIAN_POINT ( 'NONE',  ( 7.500000000000000000, 5.196152422706624918, 8.999999999999998224 ) ) ;
#5514=DIRECTION ( 'NONE',  ( 1.000000000000000000, 0.000000000000000000, -0.000000000000000000 ) ) ;
#5547=ORIENTED_EDGE ( 'NONE', *, *, #11535, .T. ) ;
#5554=DIRECTION ( 'NONE',  ( 0.000000000000000000, 0.000000000000000000, 1.000000000000000000 ) ) ;
#5563=CARTESIAN_POINT ( 'NONE',  ( 0.8038475772933614261, 5.196152422706624030, -9.000000000000000000 ) ) ;
#5620=DIRECTION ( 'NONE',  ( -1.000000000000000000, -0.000000000000000000, -0.000000000000000000 ) ) ;
#5625=AXIS2_PLACEMENT_3D ( 'NONE', #11775, #11718, #390 ) ;
#5648=( GEOMETRIC_REPRESENTATION_CONTEXT ( 3 ) GLOBAL_UNCERTAINTY_ASSIGNED_CONTEXT ( ( #12226 ) ) GLOBAL_UNIT_ASSIGNED_CONTEXT ( ( #8398, #5398, #2689 ) ) REPRESENTATION_CONTEXT ( 'NONE', 'WORKASPACE' ) );
#5682=ORIENTED_EDGE ( 'NONE', *, *, #639, .T. ) ;
#5694=VECTOR ( 'NONE', #472, 1000.000000000000000 ) ;
#5704=CIRCLE ( 'NONE', #8858, 8.999999999999998224 ) ;
#5710=CARTESIAN_POINT ( 'NONE',  ( 0.5584673446548709119, -5.621163452808895400, -8.263859302085698744 ) ) ;
#5741=B_SPLINE_CURVE_WITH_KNOTS ( 'NONE', 3,
 ( #6227, #9990, #10051, #4559, #655, #3421, #1582, #4368 ),
 .UNSPECIFIED., .F., .F.,
 ( 4, 2, 2, 4 ),
 ( 0.005257893453559881088, 0.006567392922673219099, 0.007876892391786557979, 0.01049589133001323227 ),
 .UNSPECIFIED. ) ;
#5792=ORIENTED_EDGE ( 'NONE', *, *, #3282, .T. ) ;
#5830=VERTEX_POINT ( 'NONE', #4292 ) ;
#5836=ORIENTED_EDGE ( 'NONE', *, *, #6479, .F. ) ;
#5845=DIRECTION ( 'NONE',  ( -0.000000000000000000, 1.000000000000000000, 1.669238443041288415E-16 ) ) ;
#5869=AXIS2_PLACEMENT_3D ( 'NONE', #3284, #10710, #1321 ) ;
#5872=EDGE_CURVE ( 'NONE', #11388, #8092, #3345, .T. ) ;
#5893=VERTEX_POINT ( 'NONE', #5086 ) ;
#5904=EDGE_LOOP ( 'NONE', ( #6825, #7169 ) ) ;
#5906=CARTESIAN_POINT ( 'NONE',  ( 0.01885174614367843282, 0.8831628875414415658, -9.000000000000001776 ) ) ;
#5924=CARTESIAN_POINT ( 'NONE',  ( 7.500000000000000000, -5.196152422706605378, 8.999999999999998224 ) ) ;
#5936=B_SPLINE_CURVE_WITH_KNOTS ( 'NONE', 3,
 ( #2748, #3531, #4481, #1763, #8255, #3733, #3595, #3668 ),
 .UNSPECIFIED., .F., .F.,
 ( 4, 2, 2, 4 ),
 ( 0.01498083277331294615, 0.01629713195395221526, 0.01761343113459148610, 0.02024602949587002432 ),
 .UNSPECIFIED. ) ;
#5958=ORIENTED_EDGE ( 'NONE', *, *, #5002, .F. ) ;
#5962=PRODUCT_CONTEXT ( 'NONE', #426, 'mechanical' ) ;
#5995=ADVANCED_FACE ( 'NONE', ( #2549 ), #10339, .T. ) ;
#6002=CIRCLE ( 'NONE', #9561, 5.999999999999999112 ) ;
#6005=CARTESIAN_POINT ( 'NONE',  ( 0.5595136366745770973, -4.349754824376205420, -9.000000000000001776 ) ) ;
#6006=CARTESIAN_POINT ( 'NONE',  ( 0.8038475772933637575, -10.39230484541326405, -2.038422702671202938E-16 ) ) ;
#6021=ORIENTED_EDGE ( 'NONE', *, *, #2927, .F. ) ;
#6044=DIRECTION ( 'NONE',  ( 0.000000000000000000, 0.000000000000000000, -1.000000000000000000 ) ) ;
#6049=VECTOR ( 'NONE', #6999, 1000.000000000000000 ) ;
#6058=ORIENTED_EDGE ( 'NONE', *, *, #5122, .F. ) ;
#6063=CARTESIAN_POINT ( 'NONE',  ( 0.000000000000000000, 0.000000000000000000, 0.000000000000000000 ) ) ;
#6083=EDGE_CURVE ( 'NONE', #7020, #8838, #8150, .T. ) ;
#6087=EDGE_CURVE ( 'NONE', #11020, #5893, #2826, .T. ) ;
#6117=ORIENTED_EDGE ( 'NONE', *, *, #7730, .T. ) ;
#6125=CARTESIAN_POINT ( 'NONE',  ( 0.8038475772933606489, 5.196152422706624918, 8.999999999999998224 ) ) ;
#6144=CARTESIAN_POINT ( 'NONE',  ( 0.3563104543936323476, 6.049278984716039531, 7.522341449313131534 ) ) ;
#6166=ADVANCED_FACE ( 'NONE', ( #2871 ), #11576, .T. ) ;
#6169=CIRCLE ( 'NONE', #4131, 8.999999999999998224 ) ;
#6174=DIRECTION ( 'NONE',  ( 1.000000000000000000, 0.000000000000000000, 0.000000000000000000 ) ) ;
#6178=DIRECTION ( 'NONE',  ( 0.000000000000000000, 0.000000000000000000, -1.000000000000000000 ) ) ;
#6181=VERTEX_POINT ( 'NONE', #71 ) ;
#6182=ADVANCED_FACE ( 'NONE', ( #6631 ), #3849, .F. ) ;
#6196=VECTOR ( 'NONE', #6432, 1000.000000000000000 ) ;
#6197=PLANE ( 'NONE',  #2626 ) ;
#6206=AXIS2_PLACEMENT_3D ( 'NONE', #6730, #937, #8715 ) ;
#6208=CARTESIAN_POINT ( 'NONE',  ( 7.500000000000000000, 8.082668874372530033E-16, 6.599999999999998757 ) ) ;
#6227=CARTESIAN_POINT ( 'NONE',  ( 0.000000000000000000, 7.794228634059941818, 4.500000000000007994 ) ) ;
#6257=ADVANCED_FACE ( 'NONE', ( #7738 ), #8767, .F. ) ;
#6281=CARTESIAN_POINT ( 'NONE',  ( 6.899999999999999467, -5.196152422706638241, -9.000000000000001776 ) ) ;
#6291=CARTESIAN_POINT ( 'NONE',  ( 6.899999999999999467, 10.39230484541326938, 0.000000000000000000 ) ) ;
#6294=DIRECTION ( 'NONE',  ( 0.000000000000000000, 0.000000000000000000, -1.000000000000000000 ) ) ;
#6305=DIRECTION ( 'NONE',  ( 0.000000000000000000, -1.000000000000000000, 0.000000000000000000 ) ) ;
#6327=DIRECTION ( 'NONE',  ( -0.000000000000000000, 0.000000000000000000, -1.000000000000000000 ) ) ;
#6353=CARTESIAN_POINT ( 'NONE',  ( 8.099999999999999645, 0.000000000000000000, -6.599999999999998757 ) ) ;
#6354=VECTOR ( 'NONE', #1593, 999.9999999999998863 ) ;
#6363=CARTESIAN_POINT ( 'NONE',  ( -1.234974037096769894E-14, -8.236864015571812914, 3.733333029993799901 ) ) ;
#6395=EDGE_CURVE ( 'NONE', #9788, #6696, #267, .T. ) ;
#6416=CARTESIAN_POINT ( 'NONE',  ( 57.50000000000000000, 0.000000000000000000, 0.000000000000000000 ) ) ;
#6432=DIRECTION ( 'NONE',  ( 0.000000000000000000, 0.4999999999999995004, -0.8660254037844389297 ) ) ;
#6435=VERTEX_POINT ( 'NONE', #6006 ) ;
#6446=EDGE_CURVE ( 'NONE', #4859, #5830, #9862, .T. ) ;
#6453=CARTESIAN_POINT ( 'NONE',  ( 0.5590800469813528295, -5.620102221249794638, 8.265697409064607371 ) ) ;
#6479=EDGE_CURVE ( 'NONE', #9727, #1813, #7055, .T. ) ;
#6482=AXIS2_PLACEMENT_3D ( 'NONE', #1776, #11171, #9117 ) ;
#6495=CARTESIAN_POINT ( 'NONE',  ( 7.500000000000000000, -10.39230484541326405, 0.000000000000000000 ) ) ;
#6522=ORIENTED_EDGE ( 'NONE', *, *, #6087, .T. ) ;
#6524=SHAPE_REPRESENTATION_RELATIONSHIP ( 'NONE' , 'NONE' ,  #1102, #4718 ) ;
#6530=EDGE_CURVE ( 'NONE', #1499, #9384, #8164, .T. ) ;
#6541=DIRECTION ( 'NONE',  ( -1.000000000000000000, -0.000000000000000000, -0.000000000000000000 ) ) ;
#6566=ORIENTED_EDGE ( 'NONE', *, *, #8266, .T. ) ;
#6579=DIRECTION ( 'NONE',  ( -0.000000000000000000, 0.000000000000000000, -1.000000000000000000 ) ) ;
#6591=CARTESIAN_POINT ( 'NONE',  ( 57.50000000000000000, 0.000000000000000000, 0.000000000000000000 ) ) ;
#6597=AXIS2_PLACEMENT_3D ( 'NONE', #3272, #11642, #1253 ) ;
#6598=ORIENTED_EDGE ( 'NONE', *, *, #8266, .F. ) ;
#6600=EDGE_CURVE ( 'NONE', #8092, #4400, #11260, .T. ) ;
#6625=MECHANICAL_DESIGN_GEOMETRIC_PRESENTATION_REPRESENTATION('',(#9778),#1111);
#6631=FACE_OUTER_BOUND ( 'NONE', #10439, .T. ) ;
#6640=DIRECTION ( 'NONE',  ( -1.000000000000000000, -0.000000000000000000, -0.000000000000000000 ) ) ;
#6655=PRODUCT_DEFINITION_CONTEXT ( 'detailed design', #1016, 'design' ) ;
#6661=ORIENTED_EDGE ( 'NONE', *, *, #11821, .T. ) ;
#6696=VERTEX_POINT ( 'NONE', #2849 ) ;
#6708=ORIENTED_EDGE ( 'NONE', *, *, #4290, .T. ) ;
#6716=DIRECTION ( 'NONE',  ( -1.000000000000000000, -0.000000000000000000, -0.000000000000000000 ) ) ;
#6730=CARTESIAN_POINT ( 'NONE',  ( 7.500000000000000000, 0.000000000000000000, 0.000000000000000000 ) ) ;
#6747=EDGE_CURVE ( 'NONE', #8838, #7020, #8777, .T. ) ;
#6757=EDGE_LOOP ( 'NONE', ( #5682, #6522 ) ) ;
#6761=DIRECTION ( 'NONE',  ( -1.000000000000000000, -0.000000000000000000, -0.000000000000000000 ) ) ;
#6763=ORIENTED_EDGE ( 'NONE', *, *, #2513, .F. ) ;
#6777=FILL_AREA_STYLE ('',( #7957 ) ) ;
#6786=CARTESIAN_POINT ( 'NONE',  ( 57.50000000000000000, 0.000000000000000000, 5.035999999999999588 ) ) ;
#6825=ORIENTED_EDGE ( 'NONE', *, *, #6395, .F. ) ;
#6830=VERTEX_POINT ( 'NONE', #4937 ) ;
#6839=EDGE_CURVE ( 'NONE', #11763, #11346, #1282, .T. ) ;
#6856=CARTESIAN_POINT ( 'NONE',  ( 0.8038475772933666441, 10.39230484541326938, -2.501782431774985704E-16 ) ) ;
#6914=LINE ( 'NONE', #11563, #11163 ) ;
#6915=ORIENTED_EDGE ( 'NONE', *, *, #5063, .F. ) ;
#6925=FACE_OUTER_BOUND ( 'NONE', #6983, .T. ) ;
#6932=CARTESIAN_POINT ( 'NONE',  ( 0.000000000000000000, 0.000000000000000000, 0.000000000000000000 ) ) ;
#6933=CARTESIAN_POINT ( 'NONE',  ( 0.07568653364057612021, -1.751902528125329539, -9.000000000000001776 ) ) ;
#6948=EDGE_LOOP ( 'NONE', ( #9662, #10026, #1154 ) ) ;
#6968=ORIENTED_EDGE ( 'NONE', *, *, #6083, .T. ) ;
#6983=EDGE_LOOP ( 'NONE', ( #9110, #716, #9721 ) ) ;
#6999=DIRECTION ( 'NONE',  ( 0.000000000000000000, -0.5000000000000009992, 0.8660254037844380415 ) ) ;
#7011=DIRECTION ( 'NONE',  ( 0.000000000000000000, 0.000000000000000000, 1.000000000000000000 ) ) ;
#7014=COLOUR_RGB ( '', 0.40784314, 0.44705882, 0.49803922) ;
#7020=VERTEX_POINT ( 'NONE', #10046 ) ;
#7037=DIRECTION ( 'NONE',  ( 0.000000000000000000, -0.4999999999999995004, 0.8660254037844389297 ) ) ;
#7055=B_SPLINE_CURVE_WITH_KNOTS ( 'NONE', 3,
 ( #2531, #1801, #7361, #1604, #880, #746, #816, #5563 ),
 .UNSPECIFIED., .F., .F.,
 ( 4, 2, 2, 4 ),
 ( 0.005257893453559901037, 0.006567392922673234712, 0.007876892391786568387, 0.01049589133001323574 ),
 .UNSPECIFIED. ) ;
#7087=EDGE_CURVE ( 'NONE', #8092, #6181, #680, .T. ) ;
#7114=B_SPLINE_CURVE_WITH_KNOTS ( 'NONE', 3,
 ( #9170, #8451, #12085, #4612, #7383, #2681, #6453, #641 ),
 .UNSPECIFIED., .F., .F.,
 ( 4, 2, 2, 4 ),
 ( 0.005257893453559908843, 0.006567392922673242518, 0.007876892391786575326, 0.01049589133001324094 ),
 .UNSPECIFIED. ) ;
#7132=CARTESIAN_POINT ( 'NONE',  ( -6.203669305690495683E-15, 7.351593252548062729, 5.266666970006212978 ) ) ;
#7163=DIRECTION ( 'NONE',  ( 0.000000000000000000, -0.5000000000000009992, 0.8660254037844380415 ) ) ;
#7169=ORIENTED_EDGE ( 'NONE', *, *, #9320, .F. ) ;
#7179=EDGE_LOOP ( 'NONE', ( #6021, #2635, #10067, #2914 ) ) ;
#7194=FACE_OUTER_BOUND ( 'NONE', #3603, .T. ) ;
#7201=CONICAL_SURFACE ( 'NONE', #5625, 9.000000000000000000, 1.047197551196600296 ) ;
#7222=DIRECTION ( 'NONE',  ( 0.000000000000000000, 0.000000000000000000, 1.000000000000000000 ) ) ;
#7249=EDGE_LOOP ( 'NONE', ( #2704, #7341, #5836, #12194, #9467, #5317 ) ) ;
#7295=ORIENTED_EDGE ( 'NONE', *, *, #9725, .F. ) ;
#7302=CARTESIAN_POINT ( 'NONE',  ( 6.899999999999999467, 5.196152422706624918, 8.999999999999998224 ) ) ;
#7327=DIRECTION ( 'NONE',  ( 1.000000000000000000, 0.000000000000000000, -0.000000000000000000 ) ) ;
#7341=ORIENTED_EDGE ( 'NONE', *, *, #10937, .T. ) ;
#7361=CARTESIAN_POINT ( 'NONE',  ( 0.01899995639453445906, 7.352259170992713422, -5.265513565426380715 ) ) ;
#7383=CARTESIAN_POINT ( 'NONE',  ( 0.1469846612282405540, -6.696526368584445166, 6.401276095386996268 ) ) ;
#7389=DIRECTION ( 'NONE',  ( -1.000000000000000000, -0.000000000000000000, -0.000000000000000000 ) ) ;
#7420=DIRECTION ( 'NONE',  ( 0.000000000000000000, -0.5000000000000018874, -0.8660254037844375974 ) ) ;
#7435=EDGE_CURVE ( 'NONE', #11584, #2214, #1008, .T. ) ;
#7442=CARTESIAN_POINT ( 'NONE',  ( 6.899999999999999467, -5.196152422706606266, 8.999999999999998224 ) ) ;
#7445=CARTESIAN_POINT ( 'NONE',  ( 6.899999999999999467, 7.794228634059940042, -4.500000000000007105 ) ) ;
#7462=EDGE_CURVE ( 'NONE', #759, #9388, #10517, .T. ) ;
#7471=VERTEX_POINT ( 'NONE', #1134 ) ;
#7485=DIRECTION ( 'NONE',  ( 1.000000000000000000, 0.000000000000000000, 0.000000000000000000 ) ) ;
#7500=CARTESIAN_POINT ( 'NONE',  ( 6.899999999999999467, 8.999999999999998224, 0.000000000000000000 ) ) ;
#7540=DIRECTION ( 'NONE',  ( 0.000000000000000000, 0.000000000000000000, 1.000000000000000000 ) ) ;
#7544=CARTESIAN_POINT ( 'NONE',  ( 8.099999999999999645, 0.000000000000000000, 0.000000000000000000 ) ) ;
#7551=ORIENTED_EDGE ( 'NONE', *, *, #9910, .F. ) ;
#7562=AXIS2_PLACEMENT_3D ( 'NONE', #2182, #4954, #11452 ) ;
#7565=VECTOR ( 'NONE', #8215, 1000.000000000000000 ) ;
#7578=CARTESIAN_POINT ( 'NONE',  ( 0.8038475772933614261, 5.196152422706624030, -9.000000000000000000 ) ) ;
#7583=FACE_OUTER_BOUND ( 'NONE', #8901, .T. ) ;
#7652=CARTESIAN_POINT ( 'NONE',  ( 0.3570196857253475353, -9.540868182094900618, -1.474731560294319177 ) ) ;
#7663=AXIS2_PLACEMENT_3D ( 'NONE', #6591, #1037, #4689 ) ;
#7721=DIRECTION ( 'NONE',  ( -1.000000000000000000, -0.000000000000000000, -0.000000000000000000 ) ) ;
#7730=EDGE_CURVE ( 'NONE', #6181, #9384, #4661, .T. ) ;
#7738=FACE_OUTER_BOUND ( 'NONE', #7179, .T. ) ;
#7770=( LENGTH_UNIT ( ) NAMED_UNIT ( * ) SI_UNIT ( .MILLI., .METRE. ) );
#7808=B_SPLINE_CURVE_WITH_KNOTS ( 'NONE', 3,
 ( #10015, #8105, #11931, #5308, #6363, #3510 ),
 .UNSPECIFIED., .F., .F.,
 ( 4, 2, 4 ),
 ( 2.380730968222468785E-07, 0.002629065763328365234, 0.005257893453559908843 ),
 .UNSPECIFIED. ) ;
#7809=CIRCLE ( 'NONE', #296, 5.999999999999999112 ) ;
#7858=AXIS2_PLACEMENT_3D ( 'NONE', #188, #3970, #10703 ) ;
#7894=CARTESIAN_POINT ( 'NONE',  ( 57.50000000000000000, 0.000000000000000000, 5.035999999999999588 ) ) ;
#7896=CARTESIAN_POINT ( 'NONE',  ( 7.500000000000000000, 10.39230484541326938, 0.000000000000000000 ) ) ;
#7908=CARTESIAN_POINT ( 'NONE',  ( 7.500000000000000000, 0.000000000000000000, 0.000000000000000000 ) ) ;
#7935=CIRCLE ( 'NONE', #2596, 9.000000000000000000 ) ;
#7952=EDGE_CURVE ( 'NONE', #3290, #9727, #3712, .T. ) ;
#7955=DIRECTION ( 'NONE',  ( 1.000000000000000000, 0.000000000000000000, 0.000000000000000000 ) ) ;
#7957=FILL_AREA_STYLE_COLOUR ( '', #7014 ) ;
#7963=B_SPLINE_CURVE_WITH_KNOTS ( 'NONE', 3,
 ( #2279, #2392, #6933, #10643, #6005, #2293 ),
 .UNSPECIFIED., .F., .F.,
 ( 4, 2, 4 ),
 ( 0.03045342004259713950, 0.03308352806736652996, 0.03571363609213591694 ),
 .UNSPECIFIED. ) ;
#7992=ORIENTED_EDGE ( 'NONE', *, *, #639, .F. ) ;
#7994=ORIENTED_EDGE ( 'NONE', *, *, #11, .F. ) ;
#8002=ORIENTED_EDGE ( 'NONE', *, *, #9910, .T. ) ;
#8017=DIRECTION ( 'NONE',  ( 0.000000000000000000, 0.000000000000000000, 1.000000000000000000 ) ) ;
#8047=CARTESIAN_POINT ( 'NONE',  ( -9.588412962918679838E-16, -0.8794428697894410840, 8.999999999999998224 ) ) ;
#8054=VERTEX_POINT ( 'NONE', #2183 ) ;
#8055=ADVANCED_FACE ( 'NONE', ( #11762 ), #1528, .T. ) ;
#8056=CARTESIAN_POINT ( 'NONE',  ( 57.50000000000000000, 0.000000000000000000, 0.000000000000000000 ) ) ;
#8062=ORIENTED_EDGE ( 'NONE', *, *, #7730, .F. ) ;
#8065=FACE_OUTER_BOUND ( 'NONE', #11942, .T. ) ;
#8071=ORIENTED_EDGE ( 'NONE', *, *, #6747, .T. ) ;
#8092=VERTEX_POINT ( 'NONE', #3042 ) ;
#8095=CARTESIAN_POINT ( 'NONE',  ( 6.899999999999999467, 10.39230484541326938, 0.000000000000000000 ) ) ;
#8105=CARTESIAN_POINT ( 'NONE',  ( 0.5584673446549132114, -9.967293815311096594, 0.7361406979141401630 ) ) ;
#8150=CIRCLE ( 'NONE', #2230, 5.999999999999999112 ) ;
#8164=LINE ( 'NONE', #7302, #11537 ) ;
#8186=AXIS2_PLACEMENT_3D ( 'NONE', #11952, #2425, #7011 ) ;
#8199=AXIS2_PLACEMENT_3D ( 'NONE', #6495, #4336, #11068 ) ;
#8204=ORIENTED_EDGE ( 'NONE', *, *, #3839, .T. ) ;
#8214=ORIENTED_EDGE ( 'NONE', *, *, #8496, .T. ) ;
#8215=DIRECTION ( 'NONE',  ( -1.000000000000000000, -0.000000000000000000, -0.000000000000000000 ) ) ;
#8231=LINE ( 'NONE', #10377, #8669 ) ;
#8241=CARTESIAN_POINT ( 'NONE',  ( 0.000000000000000000, -7.794228634059949812, -4.499999999999995559 ) ) ;
#8255=CARTESIAN_POINT ( 'NONE',  ( 0.1482032042127243432, 2.204400401860217240, 8.999999999999998224 ) ) ;
#8266=EDGE_CURVE ( 'NONE', #9384, #2064, #4511, .T. ) ;
#8296=ORIENTED_EDGE ( 'NONE', *, *, #7087, .F. ) ;
#8297=LINE ( 'NONE', #5499, #9856 ) ;
#8301=CARTESIAN_POINT ( 'NONE',  ( 0.07661102881317642666, 8.673996836102549679, -2.976196775178694853 ) ) ;
#8308=CARTESIAN_POINT ( 'NONE',  ( 0.8038475772933637575, -10.39230484541326405, -2.038422702671202938E-16 ) ) ;
#8315=DIRECTION ( 'NONE',  ( 0.000000000000000000, 0.000000000000000000, -1.000000000000000000 ) ) ;
#8342=ORIENTED_EDGE ( 'NONE', *, *, #10225, .F. ) ;
#8348=CARTESIAN_POINT ( 'NONE',  ( 6.899999999999999467, 0.000000000000000000, 8.999999999999998224 ) ) ;
#8398=( LENGTH_UNIT ( ) NAMED_UNIT ( * ) SI_UNIT ( .MILLI., .METRE. ) );
#8399=AXIS2_PLACEMENT_3D ( 'NONE', #1038, #9615, #9098 ) ;
#8418=AXIS2_PLACEMENT_3D ( 'NONE', #9600, #9228, #10891 ) ;
#8419=AXIS2_PLACEMENT_3D ( 'NONE', #10848, #4247, #8017 ) ;
#8449=DIRECTION ( 'NONE',  ( 1.000000000000000000, 0.000000000000000000, -0.000000000000000000 ) ) ;
#8451=CARTESIAN_POINT ( 'NONE',  ( -1.248124223602892907E-14, -7.573738413550446857, 4.881900264494497321 ) ) ;
#8477=CARTESIAN_POINT ( 'NONE',  ( 0.000000000000000000, 1.102182119232617517E-15, -8.999999999999998224 ) ) ;
#8496=EDGE_CURVE ( 'NONE', #11020, #11584, #3760, .T. ) ;
#8499=EDGE_LOOP ( 'NONE', ( #9501, #4410, #4805 ) ) ;
#8501=DIRECTION ( 'NONE',  ( 1.000000000000000000, 0.000000000000000000, -0.000000000000000000 ) ) ;
#8559=CARTESIAN_POINT ( 'NONE',  ( 0.000000000000000000, -7.794228634059949812, -4.499999999999995559 ) ) ;
#8573=ADVANCED_FACE ( 'NONE', ( #1977 ), #5092, .T. ) ;
#8582=CARTESIAN_POINT ( 'NONE',  ( -3.373308712440251100E-15, -8.014718854569432338, -4.118099735505507120 ) ) ;
#8622=DIRECTION ( 'NONE',  ( -1.000000000000000000, -0.000000000000000000, -0.000000000000000000 ) ) ;
#8624=EDGE_LOOP ( 'NONE', ( #2148, #7992, #1357, #8062, #8296, #1626 ) ) ;
#8641=ORIENTED_EDGE ( 'NONE', *, *, #9663, .T. ) ;
#8657=CARTESIAN_POINT ( 'NONE',  ( 0.000000000000000000, 1.502314598737159426E-15, -9.000000000000000000 ) ) ;
#8663=ADVANCED_FACE ( 'NONE', ( #10672 ), #1347, .F. ) ;
#8669=VECTOR ( 'NONE', #5620, 1000.000000000000000 ) ;
#8678=DIRECTION ( 'NONE',  ( 1.000000000000000000, 0.000000000000000000, -0.000000000000000000 ) ) ;
#8681=CONICAL_SURFACE ( 'NONE', #4915, 9.000000000000000000, 1.047197551196600296 ) ;
#8714=CIRCLE ( 'NONE', #1591, 8.999999999999998224 ) ;
#8715=DIRECTION ( 'NONE',  ( 0.000000000000000000, 0.000000000000000000, -1.000000000000000000 ) ) ;
#8754=AXIS2_PLACEMENT_3D ( 'NONE', #11745, #3259, #7037 ) ;
#8767=TOROIDAL_SURFACE ( 'NONE', #76, 6.599999999999998757, 0.5999999999999999778 ) ;
#8777=CIRCLE ( 'NONE', #1668, 5.999999999999999112 ) ;
#8796=ORIENTED_EDGE ( 'NONE', *, *, #6083, .F. ) ;
#8838=VERTEX_POINT ( 'NONE', #5070 ) ;
#8858=AXIS2_PLACEMENT_3D ( 'NONE', #11198, #6640, #7540 ) ;
#8864=CARTESIAN_POINT ( 'NONE',  ( 0.3593302862866777914, 3.504574740661188237, -9.000000000000001776 ) ) ;
#8872=ORIENTED_EDGE ( 'NONE', *, *, #6747, .F. ) ;
#8877=CARTESIAN_POINT ( 'NONE',  ( 7.500000000000000000, 10.39230484541326938, 0.000000000000000000 ) ) ;
#8879=DIRECTION ( 'NONE',  ( -1.000000000000000000, -0.000000000000000000, 0.000000000000000000 ) ) ;
#8887=PLANE ( 'NONE',  #8754 ) ;
#8901=EDGE_LOOP ( 'NONE', ( #4160, #8214, #10596, #3616, #6598, #10525 ) ) ;
#8902=CIRCLE ( 'NONE', #3573, 9.000000000000000000 ) ;
#8959=CARTESIAN_POINT ( 'NONE',  ( 0.8038475772933552088, -5.196152422706605378, 8.999999999999998224 ) ) ;
#8976=ORIENTED_EDGE ( 'NONE', *, *, #3203, .T. ) ;
#9006=DIRECTION ( 'NONE',  ( 1.000000000000000000, 0.000000000000000000, -0.000000000000000000 ) ) ;
#9020=CONICAL_SURFACE ( 'NONE', #4297, 9.000000000000000000, 1.047197551196600296 ) ;
#9025=EDGE_LOOP ( 'NONE', ( #9181, #5254, #8002 ) ) ;
#9048=CARTESIAN_POINT ( 'NONE',  ( 0.000000000000000000, 0.000000000000000000, 0.000000000000000000 ) ) ;
#9059=CIRCLE ( 'NONE', #10645, 9.000000000000000000 ) ;
#9098=DIRECTION ( 'NONE',  ( 0.000000000000000000, 0.000000000000000000, -1.000000000000000000 ) ) ;
#9110=ORIENTED_EDGE ( 'NONE', *, *, #5122, .T. ) ;
#9117=DIRECTION ( 'NONE',  ( 0.000000000000000000, 0.000000000000000000, -1.000000000000000000 ) ) ;
#9119=EDGE_CURVE ( 'NONE', #5893, #9384, #4996, .T. ) ;
#9125=CARTESIAN_POINT ( 'NONE',  ( 7.500000000000000000, -5.196152422706638241, -9.000000000000001776 ) ) ;
#9170=CARTESIAN_POINT ( 'NONE',  ( 0.000000000000000000, -7.794228634059935601, 4.500000000000016875 ) ) ;
#9180=CARTESIAN_POINT ( 'NONE',  ( 7.500000000000000000, 5.196152422706624030, -9.000000000000000000 ) ) ;
#9181=ORIENTED_EDGE ( 'NONE', *, *, #6446, .T. ) ;
#9182=DIRECTION ( 'NONE',  ( 0.000000000000000000, 0.000000000000000000, -1.000000000000000000 ) ) ;
#9186=CARTESIAN_POINT ( 'NONE',  ( 0.000000000000000000, 0.000000000000000000, 0.000000000000000000 ) ) ;
#9213=ORIENTED_EDGE ( 'NONE', *, *, #12147, .F. ) ;
#9228=DIRECTION ( 'NONE',  ( -1.000000000000000000, -0.000000000000000000, -0.000000000000000000 ) ) ;
#9253=CARTESIAN_POINT ( 'NONE',  ( 6.899999999999999467, 5.196152422706624030, -9.000000000000000000 ) ) ;
#9258=AXIS2_PLACEMENT_3D ( 'NONE', #6063, #11575, #5132 ) ;
#9265=ADVANCED_FACE ( 'NONE', ( #3147 ), #9020, .T. ) ;
#9294=DIRECTION ( 'NONE',  ( 1.000000000000000000, 0.000000000000000000, 0.000000000000000000 ) ) ;
#9299=CARTESIAN_POINT ( 'NONE',  ( 7.500000000000000000, 10.39230484541327115, -2.602085213965207092E-15 ) ) ;
#9320=EDGE_CURVE ( 'NONE', #6696, #9788, #1734, .T. ) ;
#9384=VERTEX_POINT ( 'NONE', #8348 ) ;
#9388=VERTEX_POINT ( 'NONE', #6291 ) ;
#9390=AXIS2_PLACEMENT_3D ( 'NONE', #9180, #12024, #3539 ) ;
#9400=FACE_OUTER_BOUND ( 'NONE', #4303, .T. ) ;
#9401=DIRECTION ( 'NONE',  ( 0.000000000000000000, 0.000000000000000000, 1.000000000000000000 ) ) ;
#9411=VERTEX_POINT ( 'NONE', #11980 ) ;
#9418=DIRECTION ( 'NONE',  ( 0.000000000000000000, 0.000000000000000000, -1.000000000000000000 ) ) ;
#9460=ORIENTED_EDGE ( 'NONE', *, *, #3602, .F. ) ;
#9467=ORIENTED_EDGE ( 'NONE', *, *, #504, .F. ) ;
#9501=ORIENTED_EDGE ( 'NONE', *, *, #6600, .T. ) ;
#9561=AXIS2_PLACEMENT_3D ( 'NONE', #1877, #5514, #8315 ) ;
#9589=CIRCLE ( 'NONE', #8419, 8.999999999999998224 ) ;
#9600=CARTESIAN_POINT ( 'NONE',  ( 6.899999999999999467, 0.000000000000000000, 0.000000000000000000 ) ) ;
#9615=DIRECTION ( 'NONE',  ( 1.000000000000000000, 0.000000000000000000, 0.000000000000000000 ) ) ;
#9629=B_SPLINE_CURVE_WITH_KNOTS ( 'NONE', 3,
 ( #1023, #5710, #1089, #3736, #1948, #8559 ),
 .UNSPECIFIED., .F., .F.,
 ( 4, 2, 4 ),
 ( 2.380730970505090229E-07, 0.002629065763328472353, 0.005257893453559894098 ),
 .UNSPECIFIED. ) ;
#9662=ORIENTED_EDGE ( 'NONE', *, *, #2693, .T. ) ;
#9663=EDGE_CURVE ( 'NONE', #2064, #1499, #9964, .T. ) ;
#9675=ORIENTED_EDGE ( 'NONE', *, *, #68, .F. ) ;
#9701=FACE_OUTER_BOUND ( 'NONE', #12065, .T. ) ;
#9721=ORIENTED_EDGE ( 'NONE', *, *, #7087, .T. ) ;
#9725=EDGE_CURVE ( 'NONE', #12174, #9411, #3395, .T. ) ;
#9727=VERTEX_POINT ( 'NONE', #10897 ) ;
#9729=AXIS2_PLACEMENT_3D ( 'NONE', #3783, #8501, #2000 ) ;
#9754=DIRECTION ( 'NONE',  ( 0.000000000000000000, -1.000000000000000000, 0.000000000000000000 ) ) ;
#9764=ORIENTED_EDGE ( 'NONE', *, *, #9854, .T. ) ;
#9768=CIRCLE ( 'NONE', #4839, 0.5999999999999998668 ) ;
#9772=FACE_OUTER_BOUND ( 'NONE', #2373, .T. ) ;
#9778=STYLED_ITEM ( 'NONE', ( #280 ), #11906 ) ;
#9788=VERTEX_POINT ( 'NONE', #7894 ) ;
#9813=TOROIDAL_SURFACE ( 'NONE', #11217, 6.599999999999998757, 0.5999999999999999778 ) ;
#9845=ADVANCED_FACE ( 'NONE', ( #705, #4417 ), #4673, .T. ) ;
#9854=EDGE_CURVE ( 'NONE', #5830, #12174, #5936, .T. ) ;
#9856=VECTOR ( 'NONE', #4583, 1000.000000000000000 ) ;
#9862=B_SPLINE_CURVE_WITH_KNOTS ( 'NONE', 3,
 ( #8959, #489, #10875, #4278, #8047, #11816 ),
 .UNSPECIFIED., .F., .F.,
 ( 4, 2, 4 ),
 ( 0.009719890944573138583, 0.01235036185894304236, 0.01498083277331294615 ),
 .UNSPECIFIED. ) ;
#9866=ORIENTED_EDGE ( 'NONE', *, *, #5063, .T. ) ;
#9881=ADVANCED_FACE ( 'NONE', ( #2613 ), #840, .F. ) ;
#9910=EDGE_CURVE ( 'NONE', #8054, #4859, #7114, .T. ) ;
#9925=LINE ( 'NONE', #2443, #4895 ) ;
#9930=DIRECTION ( 'NONE',  ( 1.000000000000000000, 0.000000000000000000, -0.000000000000000000 ) ) ;
#9938=DIRECTION ( 'NONE',  ( 0.000000000000000000, 0.000000000000000000, -1.000000000000000000 ) ) ;
#9941=DIRECTION ( 'NONE',  ( -1.000000000000000000, -0.000000000000000000, -0.000000000000000000 ) ) ;
#9964=LINE ( 'NONE', #11767, #6049 ) ;
#9990=CARTESIAN_POINT ( 'NONE',  ( -6.165341064827238593E-15, 8.014718854569425233, 4.118099735505519554 ) ) ;
#10003=LINE ( 'NONE', #5418, #6354 ) ;
#10015=CARTESIAN_POINT ( 'NONE',  ( 0.8038475772933637575, -10.39230484541326405, -2.038422702671202938E-16 ) ) ;
#10026=ORIENTED_EDGE ( 'NONE', *, *, #3212, .T. ) ;
#10027=VECTOR ( 'NONE', #6541, 1000.000000000000000 ) ;
#10046=CARTESIAN_POINT ( 'NONE',  ( 56.53599999999998715, 0.000000000000000000, 5.999999999999999112 ) ) ;
#10047=FACE_OUTER_BOUND ( 'NONE', #7249, .T. ) ;
#10051=CARTESIAN_POINT ( 'NONE',  ( 0.01899995639453432028, 8.236198097127171991, 3.734486434573631719 ) ) ;
#10067=ORIENTED_EDGE ( 'NONE', *, *, #6839, .F. ) ;
#10125=DIRECTION ( 'NONE',  ( 1.000000000000000000, 0.000000000000000000, 0.000000000000000000 ) ) ;
#10161=CARTESIAN_POINT ( 'NONE',  ( 0.000000000000000000, 10.39230484541327115, -2.602085213965207092E-15 ) ) ;
#10183=ORIENTED_EDGE ( 'NONE', *, *, #4290, .F. ) ;
#10218=CIRCLE ( 'NONE', #5869, 0.5999999999999998668 ) ;
#10225=EDGE_CURVE ( 'NONE', #3523, #6435, #4009, .T. ) ;
#10230=LINE ( 'NONE', #4487, #12080 ) ;
#10235=AXIS2_PLACEMENT_3D ( 'NONE', #11983, #9941, #4271 ) ;
#10323=ORIENTED_EDGE ( 'NONE', *, *, #3282, .F. ) ;
#10330=EDGE_CURVE ( 'NONE', #1813, #3290, #607, .T. ) ;
#10331=VERTEX_POINT ( 'NONE', #4230 ) ;
#10339=PLANE ( 'NONE',  #12102 ) ;
#10341=DIRECTION ( 'NONE',  ( 0.000000000000000000, 0.000000000000000000, -1.000000000000000000 ) ) ;
#10365=CARTESIAN_POINT ( 'NONE',  ( 6.899999999999999467, 7.794228634059940042, 4.500000000000007105 ) ) ;
#10377=CARTESIAN_POINT ( 'NONE',  ( 0.000000000000000000, 0.000000000000000000, 5.999999999999999112 ) ) ;
#10396=CARTESIAN_POINT ( 'NONE',  ( 7.500000000000000000, 5.196152422706624030, -9.000000000000000000 ) ) ;
#10399=CARTESIAN_POINT ( 'NONE',  ( 0.000000000000000000, 0.000000000000000000, 0.000000000000000000 ) ) ;
#10402=ADVANCED_FACE ( 'NONE', ( #1456 ), #738, .T. ) ;
#10420=FACE_OUTER_BOUND ( 'NONE', #5176, .T. ) ;
#10422=DIRECTION ( 'NONE',  ( 0.000000000000000000, -1.000000000000000000, 0.000000000000000000 ) ) ;
#10426=CYLINDRICAL_SURFACE ( 'NONE', #2851, 8.999999999999998224 ) ;
#10439=EDGE_LOOP ( 'NONE', ( #10617, #10694, #9460, #11502, #3061, #4958 ) ) ;
#10488=CARTESIAN_POINT ( 'NONE',  ( 6.899999999999999467, 5.196152422706624030, -9.000000000000000000 ) ) ;
#10512=ORIENTED_EDGE ( 'NONE', *, *, #7952, .F. ) ;
#10517=LINE ( 'NONE', #4664, #96 ) ;
#10525=ORIENTED_EDGE ( 'NONE', *, *, #9119, .F. ) ;
#10531=ADVANCED_FACE ( 'NONE', ( #6925 ), #11570, .T. ) ;
#10546=AXIS2_PLACEMENT_3D ( 'NONE', #11471, #6761, #1155 ) ;
#10552=SURFACE_STYLE_FILL_AREA ( #6777 ) ;
#10569=CARTESIAN_POINT ( 'NONE',  ( 7.500000000000000000, 0.000000000000000000, -6.599999999999998757 ) ) ;
#10587=ORIENTED_EDGE ( 'NONE', *, *, #7462, .T. ) ;
#10596=ORIENTED_EDGE ( 'NONE', *, *, #3212, .F. ) ;
#10602=CARTESIAN_POINT ( 'NONE',  ( 0.09318607064170508769, 1.767053008316833651, -9.000000000000001776 ) ) ;
#10613=ORIENTED_EDGE ( 'NONE', *, *, #7952, .T. ) ;
#10617=ORIENTED_EDGE ( 'NONE', *, *, #389, .F. ) ;
#10643=CARTESIAN_POINT ( 'NONE',  ( 0.3552109633437127156, -3.484997970589502447, -9.000000000000000000 ) ) ;
#10645=AXIS2_PLACEMENT_3D ( 'NONE', #5285, #9930, #5115 ) ;
#10672=FACE_OUTER_BOUND ( 'NONE', #225, .T. ) ;
#10693=CARTESIAN_POINT ( 'NONE',  ( 6.899999999999999467, 8.999999999999998224, 0.000000000000000000 ) ) ;
#10694=ORIENTED_EDGE ( 'NONE', *, *, #2021, .T. ) ;
#10701=ADVANCED_FACE ( 'NONE', ( #4419 ), #9813, .F. ) ;
#10703=DIRECTION ( 'NONE',  ( 0.000000000000000000, 0.000000000000000000, -1.000000000000000000 ) ) ;
#10710=DIRECTION ( 'NONE',  ( -0.000000000000000000, 1.000000000000000000, -1.224646799147353207E-16 ) ) ;
#10726=DIRECTION ( 'NONE',  ( -1.000000000000000000, -0.000000000000000000, -0.000000000000000000 ) ) ;
#10755=EDGE_LOOP ( 'NONE', ( #10587, #1598, #3325 ) ) ;
#10768=EDGE_CURVE ( 'NONE', #10331, #11346, #10218, .T. ) ;
#10806=ORIENTED_EDGE ( 'NONE', *, *, #4322, .T. ) ;
#10826=AXIS2_PLACEMENT_3D ( 'NONE', #3625, #1789, #5554 ) ;
#10834=CLOSED_SHELL ( 'NONE', ( #6257, #2782, #4502, #5250, #9845, #11303, #8573, #1527, #5995, #6166, #4413, #11215, #10531, #11582, #4804, #9881, #3645, #10402, #9265, #3875, #11321, #8055, #6182, #1610, #11688, #11881, #8663, #12041, #10701 ) ) ;
#10848=CARTESIAN_POINT ( 'NONE',  ( 6.899999999999999467, 0.000000000000000000, 0.000000000000000000 ) ) ;
#10863=CARTESIAN_POINT ( 'NONE',  ( 0.000000000000000000, 0.000000000000000000, 0.000000000000000000 ) ) ;
#10875=CARTESIAN_POINT ( 'NONE',  ( 0.3552109633508168662, -3.484997970623485930, 8.999999999999998224 ) ) ;
#10891=DIRECTION ( 'NONE',  ( 0.000000000000000000, 0.000000000000000000, 1.000000000000000000 ) ) ;
#10895=FACE_OUTER_BOUND ( 'NONE', #260, .T. ) ;
#10897=CARTESIAN_POINT ( 'NONE',  ( 0.000000000000000000, 7.794228634059941818, -4.500000000000007994 ) ) ;
#10904=DIRECTION ( 'NONE',  ( 0.000000000000000000, 0.000000000000000000, 1.000000000000000000 ) ) ;
#10931=FACE_OUTER_BOUND ( 'NONE', #8499, .T. ) ;
#10937=EDGE_CURVE ( 'NONE', #2214, #1813, #196, .T. ) ;
#10964=DIRECTION ( 'NONE',  ( -1.000000000000000000, -0.000000000000000000, -0.000000000000000000 ) ) ;
#11020=VERTEX_POINT ( 'NONE', #1949 ) ;
#11024=CYLINDRICAL_SURFACE ( 'NONE', #8186, 5.999999999999999112 ) ;
#11057=ORIENTED_EDGE ( 'NONE', *, *, #959, .T. ) ;
#11068=DIRECTION ( 'NONE',  ( 0.000000000000000000, 0.5000000000000018874, 0.8660254037844374864 ) ) ;
#11078=DIRECTION ( 'NONE',  ( -1.000000000000000000, 0.000000000000000000, -0.000000000000000000 ) ) ;
#11159=DIRECTION ( 'NONE',  ( 0.000000000000000000, 0.000000000000000000, -1.000000000000000000 ) ) ;
#11163=VECTOR ( 'NONE', #9754, 1000.000000000000000 ) ;
#11171=DIRECTION ( 'NONE',  ( 1.000000000000000000, 0.000000000000000000, 0.000000000000000000 ) ) ;
#11198=CARTESIAN_POINT ( 'NONE',  ( 6.899999999999999467, 0.000000000000000000, 0.000000000000000000 ) ) ;
#11215=ADVANCED_FACE ( 'NONE', ( #2259 ), #2020, .T. ) ;
#11217=AXIS2_PLACEMENT_3D ( 'NONE', #2494, #7327, #11159 ) ;
#11260=LINE ( 'NONE', #12057, #6196 ) ;
#11293=AXIS2_PLACEMENT_3D ( 'NONE', #2426, #10964, #11953 ) ;
#11303=ADVANCED_FACE ( 'NONE', ( #10895 ), #11024, .T. ) ;
#11308=LINE ( 'NONE', #678, #3426 ) ;
#11321=ADVANCED_FACE ( 'NONE', ( #7194 ), #7201, .T. ) ;
#11327=VECTOR ( 'NONE', #11367, 1000.000000000000000 ) ;
#11346=VERTEX_POINT ( 'NONE', #6208 ) ;
#11349=CARTESIAN_POINT ( 'NONE',  ( 0.5612050131712165157, 4.355613924429928119, -9.000000000000001776 ) ) ;
#11367=DIRECTION ( 'NONE',  ( -1.000000000000000000, -0.000000000000000000, -0.000000000000000000 ) ) ;
#11374=ORIENTED_EDGE ( 'NONE', *, *, #11, .T. ) ;
#11388=VERTEX_POINT ( 'NONE', #5330 ) ;
#11401=CARTESIAN_POINT ( 'NONE',  ( 7.500000000000000000, 5.196152422706624030, -9.000000000000000000 ) ) ;
#11402=ORIENTED_EDGE ( 'NONE', *, *, #6446, .F. ) ;
#11415=CARTESIAN_POINT ( 'NONE',  ( 0.000000000000000000, 0.000000000000000000, 0.000000000000000000 ) ) ;
#11440=AXIS2_PLACEMENT_3D ( 'NONE', #7908, #8879, #6044 ) ;
#11446=DIRECTION ( 'NONE',  ( -0.000000000000000000, 1.000000000000000000, 1.669238443041288415E-16 ) ) ;
#11452=DIRECTION ( 'NONE',  ( 0.000000000000000000, 0.000000000000000000, -1.000000000000000000 ) ) ;
#11471=CARTESIAN_POINT ( 'NONE',  ( 6.899999999999999467, 0.000000000000000000, 0.000000000000000000 ) ) ;
#11491=LINE ( 'NONE', #6786, #4416 ) ;
#11502=ORIENTED_EDGE ( 'NONE', *, *, #10330, .F. ) ;
#11505=VECTOR ( 'NONE', #5262, 1000.000000000000000 ) ;
#11512=DIRECTION ( 'NONE',  ( 0.000000000000000000, 0.000000000000000000, -1.000000000000000000 ) ) ;
#11535=EDGE_CURVE ( 'NONE', #7471, #11763, #9768, .T. ) ;
#11537=VECTOR ( 'NONE', #6305, 1000.000000000000000 ) ;
#11563=CARTESIAN_POINT ( 'NONE',  ( 6.899999999999999467, 5.196152422706624918, 8.999999999999998224 ) ) ;
#11570=PLANE ( 'NONE',  #4298 ) ;
#11575=DIRECTION ( 'NONE',  ( -1.000000000000000000, -0.000000000000000000, -0.000000000000000000 ) ) ;
#11576=PLANE ( 'NONE',  #7562 ) ;
#11582=ADVANCED_FACE ( 'NONE', ( #10931 ), #2519, .T. ) ;
#11584=VERTEX_POINT ( 'NONE', #2461 ) ;
#11619=EDGE_LOOP ( 'NONE', ( #4945, #4066, #5547, #9675 ) ) ;
#11636=CIRCLE ( 'NONE', #9258, 9.000000000000000000 ) ;
#11642=DIRECTION ( 'NONE',  ( -1.000000000000000000, -0.000000000000000000, -0.000000000000000000 ) ) ;
#11644=CIRCLE ( 'NONE', #11440, 6.599999999999998757 ) ;
#11652=ORIENTED_EDGE ( 'NONE', *, *, #11842, .F. ) ;
#11688=ADVANCED_FACE ( 'NONE', ( #2725 ), #1606, .F. ) ;
#11707=ORIENTED_EDGE ( 'NONE', *, *, #3685, .F. ) ;
#11718=DIRECTION ( 'NONE',  ( 1.000000000000000000, 0.000000000000000000, 0.000000000000000000 ) ) ;
#11720=CARTESIAN_POINT ( 'NONE',  ( 0.000000000000000000, 7.794228634059941818, 4.500000000000007994 ) ) ;
#11725=SURFACE_STYLE_USAGE ( .BOTH. , #1169 ) ;
#11726=ORIENTED_EDGE ( 'NONE', *, *, #3788, .F. ) ;
#11735=AXIS2_PLACEMENT_3D ( 'NONE', #10396, #4781, #1939 ) ;
#11745=CARTESIAN_POINT ( 'NONE',  ( 7.500000000000000000, -5.196152422706638241, -9.000000000000001776 ) ) ;
#11762=FACE_OUTER_BOUND ( 'NONE', #3528, .T. ) ;
#11763=VERTEX_POINT ( 'NONE', #10569 ) ;
#11765=AXIS2_PLACEMENT_3D ( 'NONE', #470, #11799, #4265 ) ;
#11767=CARTESIAN_POINT ( 'NONE',  ( 6.899999999999999467, 10.39230484541326938, 0.000000000000000000 ) ) ;
#11775=CARTESIAN_POINT ( 'NONE',  ( 0.000000000000000000, 0.000000000000000000, 0.000000000000000000 ) ) ;
#11786=CARTESIAN_POINT ( 'NONE',  ( 0.000000000000000000, 0.000000000000000000, 0.000000000000000000 ) ) ;
#11799=DIRECTION ( 'NONE',  ( 0.000000000000000000, 0.000000000000000000, -1.000000000000000000 ) ) ;
#11816=CARTESIAN_POINT ( 'NONE',  ( 0.000000000000000000, 0.000000000000000000, 9.000000000000000000 ) ) ;
#11821=EDGE_CURVE ( 'NONE', #7471, #10331, #7809, .T. ) ;
#11826=CARTESIAN_POINT ( 'NONE',  ( 6.899999999999999467, 5.196152422706624918, 8.999999999999998224 ) ) ;
#11828=ORIENTED_EDGE ( 'NONE', *, *, #10225, .T. ) ;
#11841=DIRECTION ( 'NONE',  ( 1.000000000000000000, 0.000000000000000000, -0.000000000000000000 ) ) ;
#11842=EDGE_CURVE ( 'NONE', #9384, #2309, #6914, .T. ) ;
#11881=ADVANCED_FACE ( 'NONE', ( #407 ), #4195, .F. ) ;
#11890=CARTESIAN_POINT ( 'NONE',  ( 0.5584673446549119902, 5.621163452808791483, 8.263859302085860392 ) ) ;
#11906=MANIFOLD_SOLID_BREP ( 'HeadFillet', #10834 ) ;
#11931=CARTESIAN_POINT ( 'NONE',  ( 0.3563104543936312929, -9.539178283403842329, 1.477658550686872907 ) ) ;
#11937=EDGE_CURVE ( 'NONE', #2064, #759, #9589, .T. ) ;
#11942=EDGE_LOOP ( 'NONE', ( #6968, #3864, #6661, #10323 ) ) ;
#11952=CARTESIAN_POINT ( 'NONE',  ( 0.000000000000000000, 0.000000000000000000, 0.000000000000000000 ) ) ;
#11953=DIRECTION ( 'NONE',  ( 0.000000000000000000, 0.000000000000000000, 1.000000000000000000 ) ) ;
#11957=AXIS2_PLACEMENT_3D ( 'NONE', #9048, #10904, #7955 ) ;
#11980=CARTESIAN_POINT ( 'NONE',  ( 0.000000000000000000, 7.794228634059941818, 4.500000000000007994 ) ) ;
#11983=CARTESIAN_POINT ( 'NONE',  ( 6.899999999999999467, 0.000000000000000000, 0.000000000000000000 ) ) ;
#12000=AXIS2_PLACEMENT_3D ( 'NONE', #10399, #8449, #10341 ) ;
#12013=AXIS2_PLACEMENT_3D ( 'NONE', #8877, #5110, #2209 ) ;
#12024=DIRECTION ( 'NONE',  ( 0.000000000000000000, -0.8660254037844380415, 0.5000000000000009992 ) ) ;
#12033=CARTESIAN_POINT ( 'NONE',  ( 0.8038475772933552088, -5.196152422706605378, 8.999999999999998224 ) ) ;
#12041=ADVANCED_FACE ( 'NONE', ( #10047 ), #649, .F. ) ;
#12049=ORIENTED_EDGE ( 'NONE', *, *, #793, .T. ) ;
#12057=CARTESIAN_POINT ( 'NONE',  ( 6.899999999999999467, -5.196152422706638241, -9.000000000000001776 ) ) ;
#12065=EDGE_LOOP ( 'NONE', ( #2150, #6708, #8342, #2882, #691, #1907 ) ) ;
#12080=VECTOR ( 'NONE', #844, 1000.000000000000000 ) ;
#12085=CARTESIAN_POINT ( 'NONE',  ( 0.01899995639452789487, -7.352259170992700987, 5.265513565426383380 ) ) ;
#12097=EDGE_LOOP ( 'NONE', ( #2125, #4888, #1383, #11402, #12200, #11652 ) ) ;
#12102=AXIS2_PLACEMENT_3D ( 'NONE', #7500, #9294, #9418 ) ;
#12123=CARTESIAN_POINT ( 'NONE',  ( 6.899999999999999467, 0.000000000000000000, 0.000000000000000000 ) ) ;
#12147=EDGE_CURVE ( 'NONE', #8054, #3523, #5043, .T. ) ;
#12174=VERTEX_POINT ( 'NONE', #6125 ) ;
#12194=ORIENTED_EDGE ( 'NONE', *, *, #3839, .F. ) ;
#12200=ORIENTED_EDGE ( 'NONE', *, *, #2535, .F. ) ;
#12204=CARTESIAN_POINT ( 'NONE',  ( 56.53599999999998715, 0.000000000000000000, 0.000000000000000000 ) ) ;
#12226=UNCERTAINTY_MEASURE_WITH_UNIT (LENGTH_MEASURE( 1.000000000000000082E-05 ), #8398, 'distance_accuracy_value', 'NONE');
ENDSEC;
END-ISO-10303-21;
